ISO-10303-21;
HEADER;
/* Generated by software containing ST-Developer
 * from STEP Tools, Inc. (www.steptools.com) 
 */

FILE_DESCRIPTION(
/* description */ ('Independent vertical20-tooth ratchet advance with repeated integral-c
ounterweight gravity pawls, swinging drive lever, bronze sleeves and f
ully retained axle stacks.18degpertooth. Native revolutes; geometric c
ycle checking rather than automatic contact/rolling dynamics. Gravity 
closing checked from actual pawl center of mass. Backplate/foot suppor
ts unit. Fits, torque, holding force, wear and life unassigned.'),
/* implementation_level */ '2;1');

FILE_NAME(
/* name */ 'Pawl thrust washer.step',
/* time_stamp */ '2026-11-09T06:25:53-08:00',
/* author */ (''),
/* organization */ (''),
/* preprocessor_version */ 'ST-DEVELOPER v20.2',
/* originating_system */ 'Autodesk Translation Framework v15.17.0.0',
/* authorisation */ '');

FILE_SCHEMA (('AUTOMOTIVE_DESIGN { 1 0 10303 214 3 1 1 }'));
ENDSEC;

DATA;
#10=MECHANICAL_DESIGN_GEOMETRIC_PRESENTATION_REPRESENTATION('',(#135),#4643);
#107=SHAPE_REPRESENTATION_RELATIONSHIP('SRR','None',#4712,#121);
#121=ADVANCED_BREP_SHAPE_REPRESENTATION('',(#149),#4641);
#135=STYLED_ITEM('',(#4786),#149);
#149=MANIFOLD_SOLID_BREP('Body1',#2671);
#190=FACE_BOUND('',#634,.T.);
#191=FACE_BOUND('',#636,.T.);
#298=PLANE('',#3053);
#299=PLANE('',#3054);
#443=FACE_OUTER_BOUND('',#631,.T.);
#444=FACE_OUTER_BOUND('',#632,.T.);
#445=FACE_OUTER_BOUND('',#633,.T.);
#446=FACE_OUTER_BOUND('',#635,.T.);
#631=EDGE_LOOP('',(#2437,#2438,#2439,#2440));
#632=EDGE_LOOP('',(#2441,#2442,#2443,#2444));
#633=EDGE_LOOP('',(#2445));
#634=EDGE_LOOP('',(#2446));
#635=EDGE_LOOP('',(#2447));
#636=EDGE_LOOP('',(#2448));
#895=LINE('',#4554,#1157);
#896=LINE('',#4560,#1158);
#1157=VECTOR('',#3781,4.);
#1158=VECTOR('',#3788,8.);
#1233=CIRCLE('',#3048,4.);
#1234=CIRCLE('',#3049,4.);
#1235=CIRCLE('',#3051,8.);
#1236=CIRCLE('',#3052,8.);
#1453=VERTEX_POINT('',#4551);
#1454=VERTEX_POINT('',#4553);
#1455=VERTEX_POINT('',#4557);
#1456=VERTEX_POINT('',#4559);
#1783=EDGE_CURVE('',#1453,#1453,#1233,.T.);
#1784=EDGE_CURVE('',#1453,#1454,#895,.T.);
#1785=EDGE_CURVE('',#1454,#1454,#1234,.T.);
#1786=EDGE_CURVE('',#1455,#1455,#1235,.T.);
#1787=EDGE_CURVE('',#1455,#1456,#896,.T.);
#1788=EDGE_CURVE('',#1456,#1456,#1236,.T.);
#2437=ORIENTED_EDGE('',*,*,#1783,.F.);
#2438=ORIENTED_EDGE('',*,*,#1784,.T.);
#2439=ORIENTED_EDGE('',*,*,#1785,.T.);
#2440=ORIENTED_EDGE('',*,*,#1784,.F.);
#2441=ORIENTED_EDGE('',*,*,#1786,.F.);
#2442=ORIENTED_EDGE('',*,*,#1787,.T.);
#2443=ORIENTED_EDGE('',*,*,#1788,.T.);
#2444=ORIENTED_EDGE('',*,*,#1787,.F.);
#2445=ORIENTED_EDGE('',*,*,#1786,.T.);
#2446=ORIENTED_EDGE('',*,*,#1783,.T.);
#2447=ORIENTED_EDGE('',*,*,#1788,.F.);
#2448=ORIENTED_EDGE('',*,*,#1785,.F.);
#2506=CYLINDRICAL_SURFACE('',#3047,4.);
#2507=CYLINDRICAL_SURFACE('',#3050,8.);
#2649=ADVANCED_FACE('',(#443),#2506,.F.);
#2650=ADVANCED_FACE('',(#444),#2507,.T.);
#2651=ADVANCED_FACE('',(#445,#190),#298,.T.);
#2652=ADVANCED_FACE('',(#446,#191),#299,.F.);
#2671=CLOSED_SHELL('',(#2649,#2650,#2651,#2652));
#3046=AXIS2_PLACEMENT_3D('',#4549,#3775,#3776);
#3047=AXIS2_PLACEMENT_3D('',#4550,#3777,#3778);
#3048=AXIS2_PLACEMENT_3D('',#4552,#3779,#3780);
#3049=AXIS2_PLACEMENT_3D('',#4555,#3782,#3783);
#3050=AXIS2_PLACEMENT_3D('',#4556,#3784,#3785);
#3051=AXIS2_PLACEMENT_3D('',#4558,#3786,#3787);
#3052=AXIS2_PLACEMENT_3D('',#4561,#3789,#3790);
#3053=AXIS2_PLACEMENT_3D('',#4562,#3791,#3792);
#3054=AXIS2_PLACEMENT_3D('',#4563,#3793,#3794);
#3775=DIRECTION('axis',(0.,0.,1.));
#3776=DIRECTION('refdir',(1.,0.,0.));
#3777=DIRECTION('center_axis',(0.,0.,1.));
#3778=DIRECTION('ref_axis',(1.,0.,0.));
#3779=DIRECTION('center_axis',(0.,0.,-1.));
#3780=DIRECTION('ref_axis',(1.,0.,0.));
#3781=DIRECTION('',(0.,0.,-1.));
#3782=DIRECTION('center_axis',(0.,0.,-1.));
#3783=DIRECTION('ref_axis',(1.,0.,0.));
#3784=DIRECTION('center_axis',(0.,0.,1.));
#3785=DIRECTION('ref_axis',(1.,0.,0.));
#3786=DIRECTION('center_axis',(0.,0.,1.));
#3787=DIRECTION('ref_axis',(1.,0.,0.));
#3788=DIRECTION('',(0.,0.,-1.));
#3789=DIRECTION('center_axis',(0.,0.,1.));
#3790=DIRECTION('ref_axis',(1.,0.,0.));
#3791=DIRECTION('center_axis',(0.,0.,1.));
#3792=DIRECTION('ref_axis',(1.,0.,0.));
#3793=DIRECTION('center_axis',(0.,0.,1.));
#3794=DIRECTION('ref_axis',(1.,0.,0.));
#4549=CARTESIAN_POINT('',(0.,0.,0.));
#4550=CARTESIAN_POINT('Origin',(0.,0.,0.));
#4551=CARTESIAN_POINT('',(-4.,-4.89858719658941E-16,2.));
#4552=CARTESIAN_POINT('Origin',(0.,0.,2.));
#4553=CARTESIAN_POINT('',(-4.,-4.89858719658941E-16,0.));
#4554=CARTESIAN_POINT('',(-4.,-4.89858719658941E-16,0.));
#4555=CARTESIAN_POINT('Origin',(0.,0.,0.));
#4556=CARTESIAN_POINT('Origin',(0.,0.,0.));
#4557=CARTESIAN_POINT('',(-8.,-9.79717439317883E-16,2.));
#4558=CARTESIAN_POINT('Origin',(0.,0.,2.));
#4559=CARTESIAN_POINT('',(-8.,-9.79717439317883E-16,0.));
#4560=CARTESIAN_POINT('',(-8.,-9.79717439317883E-16,0.));
#4561=CARTESIAN_POINT('Origin',(0.,0.,0.));
#4562=CARTESIAN_POINT('Origin',(0.,0.,2.));
#4563=CARTESIAN_POINT('Origin',(0.,0.,0.));
#4625=UNCERTAINTY_MEASURE_WITH_UNIT(LENGTH_MEASURE(0.01),#4644,
'DISTANCE_ACCURACY_VALUE',
'Maximum model space distance between geometric entities at asserted c
onnectivities');
#4627=UNCERTAINTY_MEASURE_WITH_UNIT(LENGTH_MEASURE(0.01),#4644,
'DISTANCE_ACCURACY_VALUE',
'Maximum model space distance between geometric entities at asserted c
onnectivities');
#4641=(
GEOMETRIC_REPRESENTATION_CONTEXT(3)
GLOBAL_UNCERTAINTY_ASSIGNED_CONTEXT((#4625))
GLOBAL_UNIT_ASSIGNED_CONTEXT((#4644,#4646,#4647))
REPRESENTATION_CONTEXT('','3D')
);
#4643=(
GEOMETRIC_REPRESENTATION_CONTEXT(3)
GLOBAL_UNCERTAINTY_ASSIGNED_CONTEXT((#4627))
GLOBAL_UNIT_ASSIGNED_CONTEXT((#4644,#4646,#4647))
REPRESENTATION_CONTEXT('','3D')
);
#4644=(
LENGTH_UNIT()
NAMED_UNIT(*)
SI_UNIT(.MILLI.,.METRE.)
);
#4646=(
NAMED_UNIT(*)
PLANE_ANGLE_UNIT()
SI_UNIT($,.RADIAN.)
);
#4647=(
NAMED_UNIT(*)
SI_UNIT($,.STERADIAN.)
SOLID_ANGLE_UNIT()
);
#4661=SHAPE_DEFINITION_REPRESENTATION(#4676,#4712);
#4676=PRODUCT_DEFINITION_SHAPE('',$,#4728);
#4712=SHAPE_REPRESENTATION('',(#3046),#4641);
#4714=PRODUCT_DEFINITION_CONTEXT('part definition',#4761,'design');
#4728=PRODUCT_DEFINITION('Pawl thrust washer','Pawl thrust washer',#4743,
#4714);
#4743=PRODUCT_DEFINITION_FORMATION('',$,#4776);
#4761=APPLICATION_CONTEXT(
'Core Data for Automotive Mechanical Design Process');
#4762=PRODUCT_CONTEXT('part definition',#4761,'mechanical');
#4776=PRODUCT('Pawl thrust washer','Pawl thrust washer',$,(#4762));
#4786=PRESENTATION_STYLE_ASSIGNMENT((#4795));
#4795=SURFACE_STYLE_USAGE(.BOTH.,#4804);
#4804=SURFACE_SIDE_STYLE('',(#4813));
#4813=SURFACE_STYLE_FILL_AREA(#4822);
#4822=FILL_AREA_STYLE('Light gray',(#4831));
#4831=FILL_AREA_STYLE_COLOUR('Light gray',#4840);
#4840=COLOUR_RGB('Light gray',0.725490196078431,0.752941176470588,0.792156862745098);
ENDSEC;
END-ISO-10303-21;
